ISO-10303-21;
HEADER;
FILE_DESCRIPTION (('STEP AP214'),
    '1' );
FILE_NAME ('1.5 Handle Ball.step',
    '2026-10-06T08:51:13',
    ( '' ),
    ( '' ),
    'SwSTEP 2.0',
    'SolidWorks 2021',
    '' );
FILE_SCHEMA (( 'AUTOMOTIVE_DESIGN' ));
ENDSEC;

DATA;
#196=( LENGTH_UNIT ( ) NAMED_UNIT ( * ) SI_UNIT ( .MILLI., .METRE. ) );
#558=VERTEX_POINT ( 'NONE', #43749 ) ;
#644=EDGE_LOOP ( 'NONE', ( #63079, #95765, #122634, #54205, #52507, #92729, #71035, #105923, #46654 ) ) ;
#747=PRODUCT_DEFINITION_FORMATION_WITH_SPECIFIED_SOURCE ( 'ANY', '', #32831, .NOT_KNOWN. ) ;
#811=AXIS2_PLACEMENT_3D ( 'NONE', #14769, #3844, #59046 ) ;
#832=DIRECTION ( 'NONE',  ( 0.000000000000000000, 0.000000000000000000, 1.000000000000000000 ) ) ;
#930=SURFACE_STYLE_FILL_AREA ( #10384 ) ;
#1269=EDGE_CURVE ( 'NONE', #63821, #131899, #101132, .T. ) ;
#1358=ORIENTED_EDGE ( 'NONE', *, *, #129245, .F. ) ;
#1584=DIRECTION ( 'NONE',  ( -0.000000000000000000, -0.000000000000000000, -1.000000000000000000 ) ) ;
#1799=VERTEX_POINT ( 'NONE', #51288 ) ;
#2244=CARTESIAN_POINT ( 'NONE',  ( 0.000000000000000000, -9.500000000000000000, 0.000000000000000000 ) ) ;
#2347=FACE_BOUND ( 'NONE', #104330, .T. ) ;
#3078=CARTESIAN_POINT ( 'NONE',  ( -1.320799999999990870, 0.000000000000000000, 0.000000000000000000 ) ) ;
#3268=EDGE_CURVE ( 'NONE', #72134, #23963, #48043, .T. ) ;
#3352=EDGE_CURVE ( 'NONE', #131899, #4118, #114417, .T. ) ;
#3669=FACE_OUTER_BOUND ( 'NONE', #82346, .T. ) ;
#3844=DIRECTION ( 'NONE',  ( 0.000000000000000000, 0.000000000000000000, -1.000000000000000000 ) ) ;
#3930=STYLED_ITEM ( 'NONE', ( #74094 ), #92605 ) ;
#3972=CARTESIAN_POINT ( 'NONE',  ( 4.198949119135569656E-17, -1.320799999999990870, 4.000000000000000000 ) ) ;
#4118=VERTEX_POINT ( 'NONE', #45718 ) ;
#4844=( LENGTH_UNIT ( ) NAMED_UNIT ( * ) SI_UNIT ( .MILLI., .METRE. ) );
#4908=CARTESIAN_POINT ( 'NONE',  ( 4.000000000000000000, -8.616843969807042924, 0.000000000000000000 ) ) ;
#5521=CARTESIAN_POINT ( 'NONE',  ( 0.000000000000000000, 0.000000000000000000, 0.000000000000000000 ) ) ;
#6077=ORIENTED_EDGE ( 'NONE', *, *, #81606, .F. ) ;
#6490=CARTESIAN_POINT ( 'NONE',  ( -1.252866409880302623, 0.4270777084541245161, 3.798888653466065968 ) ) ;
#7688=STYLED_ITEM ( 'NONE', ( #107757 ), #129565 ) ;
#7853=EDGE_CURVE ( 'NONE', #58791, #30060, #70307, .T. ) ;
#7949=CARTESIAN_POINT ( 'NONE',  ( 0.000000000000000000, 0.000000000000000000, 0.000000000000000000 ) ) ;
#8109=CARTESIAN_POINT ( 'NONE',  ( 0.000000000000000000, 0.000000000000000000, 0.000000000000000000 ) ) ;
#8403=CARTESIAN_POINT ( 'NONE',  ( 0.8137007348675845408, -1.054356994394161307, 3.918334772610103212 ) ) ;
#8434=CARTESIAN_POINT ( 'NONE',  ( 0.6638242047990419170, 1.145087188747829554, 3.945200277712134884 ) ) ;
#8793=DIRECTION ( 'NONE',  ( 0.000000000000000000, 0.000000000000000000, 1.000000000000000000 ) ) ;
#8925=CARTESIAN_POINT ( 'NONE',  ( 0.000000000000000000, 0.000000000000000000, 0.000000000000000000 ) ) ;
#9122=SHAPE_REPRESENTATION_RELATIONSHIP ( 'NONE' , 'NONE' ,  #118114, #129565 ) ;
#9901=CARTESIAN_POINT ( 'NONE',  ( 1.277919311390762758, 0.3448754841691806794, 3.790415138944262186 ) ) ;
#9970=( GEOMETRIC_REPRESENTATION_CONTEXT ( 3 ) GLOBAL_UNCERTAINTY_ASSIGNED_CONTEXT ( ( #93698 ) ) GLOBAL_UNIT_ASSIGNED_CONTEXT ( ( #43256, #54845, #32367 ) ) REPRESENTATION_CONTEXT ( 'NONE', 'WORKASPACE' ) );
#10235=CIRCLE ( 'NONE', #79747, 1.320799999999990870 ) ;
#10347=CARTESIAN_POINT ( 'NONE',  ( 0.000000000000000000, 8.616843969807042924, 0.000000000000000000 ) ) ;
#10384=FILL_AREA_STYLE ('',( #90093 ) ) ;
#10710=MECHANICAL_DESIGN_GEOMETRIC_PRESENTATION_REPRESENTATION('',(#100976),#131102);
#11038=DIRECTION ( 'NONE',  ( 0.000000000000000000, -1.000000000000000000, 0.000000000000000000 ) ) ;
#11079=FACE_OUTER_BOUND ( 'NONE', #105405, .T. ) ;
#11766=DIRECTION ( 'NONE',  ( 0.000000000000000000, 0.000000000000000000, -1.000000000000000000 ) ) ;
#11785=CARTESIAN_POINT ( 'NONE',  ( -1.320800000000306618, -4.493284886149243553E-13, 3.775643966265820328 ) ) ;
#13061=EDGE_CURVE ( 'NONE', #72010, #58791, #52982, .T. ) ;
#13317=SURFACE_STYLE_FILL_AREA ( #68476 ) ;
#14769=CARTESIAN_POINT ( 'NONE',  ( 0.000000000000000000, 0.000000000000000000, 0.000000000000000000 ) ) ;
#14969=ORIENTED_EDGE ( 'NONE', *, *, #43848, .F. ) ;
#15106=CARTESIAN_POINT ( 'NONE',  ( 0.000000000000000000, 0.000000000000000000, 9.407735506486140764 ) ) ;
#15262=DIRECTION ( 'NONE',  ( -0.000000000000000000, 1.000000000000000000, -0.000000000000000000 ) ) ;
#15865=ORIENTED_EDGE ( 'NONE', *, *, #1269, .T. ) ;
#15980=EDGE_LOOP ( 'NONE', ( #6077, #108307, #76296, #79937, #127755 ) ) ;
#17009=EDGE_CURVE ( 'NONE', #131899, #48968, #102616, .T. ) ;
#17222=CARTESIAN_POINT ( 'NONE',  ( -4.000000000000000000, -8.616843969807042924, -4.898587196589412829E-16 ) ) ;
#18834=DIRECTION ( 'NONE',  ( -1.000000000000000000, 0.000000000000000000, 0.000000000000000000 ) ) ;
#18870=CARTESIAN_POINT ( 'NONE',  ( 0.000000000000000000, 0.000000000000000000, 0.000000000000000000 ) ) ;
#19105=ORIENTED_EDGE ( 'NONE', *, *, #82466, .F. ) ;
#19328=CARTESIAN_POINT ( 'NONE',  ( 0.4283298879861147102, -1.252411602983660499, 3.977815754073098287 ) ) ;
#19344=SURFACE_STYLE_USAGE ( .BOTH. , #142564 ) ;
#19778=DIRECTION ( 'NONE',  ( 0.000000000000000000, -1.000000000000000000, 0.000000000000000000 ) ) ;
#20393=FILL_AREA_STYLE_COLOUR ( '', #89656 ) ;
#20740=DIRECTION ( 'NONE',  ( -0.000000000000000000, 1.000000000000000000, -0.000000000000000000 ) ) ;
#21284=DIRECTION ( 'NONE',  ( 1.000000000000000000, 0.000000000000000000, 0.000000000000000000 ) ) ;
#22194=CARTESIAN_POINT ( 'NONE',  ( 0.3479702768469047913, 1.285727409420016176, 3.988060179666636618 ) ) ;
#22646=CARTESIAN_POINT ( 'NONE',  ( -0.3439913038278733515, -1.278150760195258862, 3.986088164604868478 ) ) ;
#23295=CYLINDRICAL_SURFACE ( 'NONE', #32658, 4.000000000000000000 ) ;
#23500=( NAMED_UNIT ( * ) SI_UNIT ( $, .STERADIAN. ) SOLID_ANGLE_UNIT ( ) );
#23754=AXIS2_PLACEMENT_3D ( 'NONE', #10347, #11038, #11766 ) ;
#23963=VERTEX_POINT ( 'NONE', #41232 ) ;
#24273=UNCERTAINTY_MEASURE_WITH_UNIT (LENGTH_MEASURE( 1.000000000000000082E-05 ), #31307, 'distance_accuracy_value', 'NONE');
#25688=UNCERTAINTY_MEASURE_WITH_UNIT (LENGTH_MEASURE( 1.000000000000000082E-05 ), #69170, 'distance_accuracy_value', 'NONE');
#26130=MECHANICAL_DESIGN_GEOMETRIC_PRESENTATION_REPRESENTATION('',(#7688),#9970);
#27328=CARTESIAN_POINT ( 'NONE',  ( 1.320799999999991092, -0.1737498520445722172, 3.775643966265890938 ) ) ;
#27603=CARTESIAN_POINT ( 'NONE',  ( -4.912274722134691121E-20, 1.320799999999990870, 4.000000000000000000 ) ) ;
#27914=DIRECTION ( 'NONE',  ( 0.000000000000000000, 0.000000000000000000, -1.000000000000000000 ) ) ;
#28066=CARTESIAN_POINT ( 'NONE',  ( 1.285559789426349520, -0.3484322621842600443, 3.788421920936591025 ) ) ;
#28315=CARTESIAN_POINT ( 'NONE',  ( -0.8730705227619277586, 0.9948348601054731732, 3.904059355167917911 ) ) ;
#29016=CARTESIAN_POINT ( 'NONE',  ( -1.311990357131797014, 0.1751088764723762181, 3.778756969498452634 ) ) ;
#29774=EDGE_LOOP ( 'NONE', ( #79820, #110728, #46331, #79855, #45116, #43925 ) ) ;
#30060=VERTEX_POINT ( 'NONE', #61216 ) ;
#30483=CARTESIAN_POINT ( 'NONE',  ( -1.320799999999990870, 0.000000000000000000, 9.407735506486140764 ) ) ;
#30957=AXIS2_PLACEMENT_3D ( 'NONE', #7949, #118127, #18834 ) ;
#31269=CARTESIAN_POINT ( 'NONE',  ( 0.000000000000000000, -9.500000000000000000, 4.000000000000000000 ) ) ;
#31307=( LENGTH_UNIT ( ) NAMED_UNIT ( * ) SI_UNIT ( .MILLI., .METRE. ) );
#31655=VERTEX_POINT ( 'NONE', #120724 ) ;
#32157=SURFACE_SIDE_STYLE ('',( #930 ) ) ;
#32367=( NAMED_UNIT ( * ) SI_UNIT ( $, .STERADIAN. ) SOLID_ANGLE_UNIT ( ) );
#32658=AXIS2_PLACEMENT_3D ( 'NONE', #2244, #15262, #832 ) ;
#32775=CIRCLE ( 'NONE', #88344, 1.320799999999990870 ) ;
#32831=PRODUCT ( '1.5 Handle Ball', '1.5 Handle Ball', '', ( #126485 ) ) ;
#33142=CARTESIAN_POINT ( 'NONE',  ( 0.8065107498756644011, 1.049489235317104807, 3.918521177239187026 ) ) ;
#33279=COLOUR_RGB ( '', 0.31764706, 0.68627451, 0.89019608) ;
#33595=CARTESIAN_POINT ( 'NONE',  ( -1.055214894802011694, -0.8126175113835719666, 3.860312914990109423 ) ) ;
#33612=( NAMED_UNIT ( * ) SI_UNIT ( $, .STERADIAN. ) SOLID_ANGLE_UNIT ( ) );
#33838=AXIS2_PLACEMENT_3D ( 'NONE', #77125, #120552, #21284 ) ;
#34220=DIRECTION ( 'NONE',  ( 0.000000000000000000, 0.000000000000000000, 1.000000000000000000 ) ) ;
#35062=CIRCLE ( 'NONE', #81314, 9.500000000000000000 ) ;
#36261=VECTOR ( 'NONE', #108770, 1000.000000000000000 ) ;
#36769=ORIENTED_EDGE ( 'NONE', *, *, #3352, .F. ) ;
#37613=DIRECTION ( 'NONE',  ( -0.000000000000000000, -0.000000000000000000, -1.000000000000000000 ) ) ;
#38071=AXIS2_PLACEMENT_3D ( 'NONE', #66507, #78806, #46205 ) ;
#38731=DIRECTION ( 'NONE',  ( -0.000000000000000000, -0.000000000000000000, -1.000000000000000000 ) ) ;
#38890=VECTOR ( 'NONE', #84290, 1000.000000000000000 ) ;
#39926=CARTESIAN_POINT ( 'NONE',  ( -1.152691986415045111, 0.6678635374937111902, 3.830955253485991197 ) ) ;
#40136=COLOUR_RGB ( '', 0.66274510, 0.83137255, 0.94901961) ;
#41232=CARTESIAN_POINT ( 'NONE',  ( -1.320800000000306618, -4.493284886149243553E-13, 3.775643966265820328 ) ) ;
#41468=DIRECTION ( 'NONE',  ( -0.000000000000000000, 1.000000000000000000, -0.000000000000000000 ) ) ;
#42052=CARTESIAN_POINT ( 'NONE',  ( -0.3480366351640904465, 1.285757288101296858, 3.988067004281481864 ) ) ;
#42199=CARTESIAN_POINT ( 'NONE',  ( 4.898587196589412829E-16, -9.500000000000000000, -4.000000000000000000 ) ) ;
#42862=VERTEX_POINT ( 'NONE', #3972 ) ;
#43256=( LENGTH_UNIT ( ) NAMED_UNIT ( * ) SI_UNIT ( .MILLI., .METRE. ) );
#43306=ORIENTED_EDGE ( 'NONE', *, *, #72048, .F. ) ;
#43543=AXIS2_PLACEMENT_3D ( 'NONE', #73412, #41468, #117576 ) ;
#43749=CARTESIAN_POINT ( 'NONE',  ( 4.898587196589412829E-16, 8.616843969807042924, -4.000000000000000000 ) ) ;
#43817=ADVANCED_FACE ( 'NONE', ( #140613 ), #139942, .F. ) ;
#43848=EDGE_CURVE ( 'NONE', #72010, #23963, #97130, .T. ) ;
#43925=ORIENTED_EDGE ( 'NONE', *, *, #17009, .F. ) ;
#43981=CARTESIAN_POINT ( 'NONE',  ( 0.8725517856990301357, 0.9952662357582434671, 3.904172814578533934 ) ) ;
#44718=FILL_AREA_STYLE ('',( #63598 ) ) ;
#45116=ORIENTED_EDGE ( 'NONE', *, *, #66223, .T. ) ;
#45194=CARTESIAN_POINT ( 'NONE',  ( -1.153248962236076647, -0.6664845763655985467, 3.830776090634477882 ) ) ;
#45718=CARTESIAN_POINT ( 'NONE',  ( 4.898587196589412829E-16, -8.616843969807042924, -4.000000000000000000 ) ) ;
#46205=DIRECTION ( 'NONE',  ( 0.000000000000000000, 0.000000000000000000, 1.000000000000000000 ) ) ;
#46331=ORIENTED_EDGE ( 'NONE', *, *, #72048, .T. ) ;
#46449=CLOSED_SHELL ( 'NONE', ( #43817, #124202, #81158, #121822, #73485, #95849 ) ) ;
#46617=CARTESIAN_POINT ( 'NONE',  ( 0.000000000000000000, 0.000000000000000000, 9.407735506486140764 ) ) ;
#46654=ORIENTED_EDGE ( 'NONE', *, *, #88000, .F. ) ;
#46749=PRESENTATION_STYLE_ASSIGNMENT (( #101774 ) ) ;
#47421=AXIS2_PLACEMENT_3D ( 'NONE', #69815, #113994, #103796 ) ;
#47801=DIRECTION ( 'NONE',  ( -1.000000000000000000, 0.000000000000000000, 0.000000000000000000 ) ) ;
#48043=LINE ( 'NONE', #3078, #128304 ) ;
#48968=VERTEX_POINT ( 'NONE', #54236 ) ;
#49640=LINE ( 'NONE', #93819, #120306 ) ;
#49844=CARTESIAN_POINT ( 'NONE',  ( 1.055465189827180295, -0.8122627595889222452, 3.860239566300592617 ) ) ;
#50976=EDGE_CURVE ( 'NONE', #1799, #31655, #49640, .T. ) ;
#51288=CARTESIAN_POINT ( 'NONE',  ( 1.320799999999990870, 1.617513492313812843E-16, 9.407735506486140764 ) ) ;
#52507=ORIENTED_EDGE ( 'NONE', *, *, #13061, .F. ) ;
#52689=CARTESIAN_POINT ( 'NONE',  ( 1.252729709573792150, 0.4274928414560493217, 3.798934289757320837 ) ) ;
#52905=DIRECTION ( 'NONE',  ( 1.224646799147353207E-16, 0.000000000000000000, -1.000000000000000000 ) ) ;
#52982=LINE ( 'NONE', #31269, #36261 ) ;
#53195=DIRECTION ( 'NONE',  ( 1.000000000000000000, 0.000000000000000000, 0.000000000000000000 ) ) ;
#53448=CIRCLE ( 'NONE', #72011, 4.000000000000000000 ) ;
#54153=EDGE_CURVE ( 'NONE', #42862, #31655, #61094, .T. ) ;
#54166=EDGE_CURVE ( 'NONE', #63821, #42862, #83161, .T. ) ;
#54205=ORIENTED_EDGE ( 'NONE', *, *, #7853, .F. ) ;
#54236=CARTESIAN_POINT ( 'NONE',  ( 4.000000000000000000, 8.616843969807042924, 0.000000000000000000 ) ) ;
#54636=( NAMED_UNIT ( * ) PLANE_ANGLE_UNIT ( ) SI_UNIT ( $, .RADIAN. ) );
#54845=( NAMED_UNIT ( * ) PLANE_ANGLE_UNIT ( ) SI_UNIT ( $, .RADIAN. ) );
#54981=DIRECTION ( 'NONE',  ( 0.000000000000000000, -1.000000000000000000, 0.000000000000000000 ) ) ;
#55577=CARTESIAN_POINT ( 'NONE',  ( -4.912274722134691121E-20, 1.320799999999990870, 4.000000000000000000 ) ) ;
#56041=DIRECTION ( 'NONE',  ( -1.000000000000000000, 0.000000000000000000, 0.000000000000000000 ) ) ;
#56185=FILL_AREA_STYLE_COLOUR ( '', #33279 ) ;
#56662=DIRECTION ( 'NONE',  ( -0.000000000000000000, 1.000000000000000000, -0.000000000000000000 ) ) ;
#56762=ORIENTED_EDGE ( 'NONE', *, *, #99598, .T. ) ;
#57591=SURFACE_SIDE_STYLE ('',( #13317 ) ) ;
#58791=VERTEX_POINT ( 'NONE', #85766 ) ;
#59046=DIRECTION ( 'NONE',  ( 1.000000000000000000, 0.000000000000000000, 0.000000000000000000 ) ) ;
#59846=CARTESIAN_POINT ( 'NONE',  ( 0.000000000000000000, 8.616843969807042924, 0.000000000000000000 ) ) ;
#61094=B_SPLINE_CURVE_WITH_KNOTS ( 'NONE', 3,
 ( #106293, #107041, #95451, #129496, #19328, #63586, #8403, #49844, #126640, #28066, #27328, #71577 ),
 .UNSPECIFIED., .F., .F.,
 ( 4, 2, 2, 2, 2, 4 ),
 ( 4.076487489278275292E-20, 0.0002600071698628363950, 0.0005200143397256725732, 0.001040028679451345146, 0.001560043019177017503, 0.002080057358902690293 ),
 .UNSPECIFIED. ) ;
#61216=CARTESIAN_POINT ( 'NONE',  ( -4.000000000000000000, 8.616843969807042924, -4.898587196589412829E-16 ) ) ;
#61668=CARTESIAN_POINT ( 'NONE',  ( -0.8069443138166949581, 1.049154855905557238, 3.918431363226604347 ) ) ;
#61832=FACE_OUTER_BOUND ( 'NONE', #644, .T. ) ;
#62233=B_SPLINE_CURVE_WITH_KNOTS ( 'NONE', 3,
 ( #11785, #66913, #110384, #45194, #33595, #111092, #121978, #122705, #108953, #79261, #22646, #76364, #132913, #120533 ),
 .UNSPECIFIED., .F., .F.,
 ( 4, 2, 2, 2, 2, 2, 4 ),
 ( 0.006237562923353405335, 0.006757314257999464183, 0.007277065592645523030, 0.007536941259968552020, 0.007796816927291581878, 0.008056692594614611735, 0.008316568261937639858 ),
 .UNSPECIFIED. ) ;
#62907=ORIENTED_EDGE ( 'NONE', *, *, #54166, .T. ) ;
#63079=ORIENTED_EDGE ( 'NONE', *, *, #71745, .F. ) ;
#63134=DIRECTION ( 'NONE',  ( -1.000000000000000000, 0.000000000000000000, -1.224646799147353207E-16 ) ) ;
#63257=FILL_AREA_STYLE ('',( #20393 ) ) ;
#63586=CARTESIAN_POINT ( 'NONE',  ( 0.6679544216110644417, -1.152520817846947043, 3.947122439933573812 ) ) ;
#63598=FILL_AREA_STYLE_COLOUR ( '', #40136 ) ;
#63821=VERTEX_POINT ( 'NONE', #142795 ) ;
#65226=PRODUCT_DEFINITION_SHAPE ( 'NONE', 'NONE',  #117397 ) ;
#65571=AXIS2_PLACEMENT_3D ( 'NONE', #65881, #54981, #131100 ) ;
#65881=CARTESIAN_POINT ( 'NONE',  ( 0.000000000000000000, 8.616843969807042924, 0.000000000000000000 ) ) ;
#66223=EDGE_CURVE ( 'NONE', #558, #48968, #97738, .T. ) ;
#66507=CARTESIAN_POINT ( 'NONE',  ( 0.000000000000000000, -8.616843969807042924, 0.000000000000000000 ) ) ;
#66913=CARTESIAN_POINT ( 'NONE',  ( -1.320799999999936025, -0.1740827700035259273, 3.775643966265910034 ) ) ;
#68062=ORIENTED_EDGE ( 'NONE', *, *, #88000, .T. ) ;
#68476=FILL_AREA_STYLE ('',( #56185 ) ) ;
#69170=( LENGTH_UNIT ( ) NAMED_UNIT ( * ) SI_UNIT ( .MILLI., .METRE. ) );
#69815=CARTESIAN_POINT ( 'NONE',  ( 0.000000000000000000, -8.616843969807042924, 0.000000000000000000 ) ) ;
#70307=CIRCLE ( 'NONE', #121155, 4.000000000000000000 ) ;
#71035=ORIENTED_EDGE ( 'NONE', *, *, #109752, .T. ) ;
#71535=FACE_OUTER_BOUND ( 'NONE', #116125, .T. ) ;
#71566=ORIENTED_EDGE ( 'NONE', *, *, #82466, .T. ) ;
#71577=CARTESIAN_POINT ( 'NONE',  ( 1.320799999999990870, 1.617513596018363294E-16, 3.775643966265890494 ) ) ;
#71745=EDGE_CURVE ( 'NONE', #4118, #123737, #53448, .T. ) ;
#72010=VERTEX_POINT ( 'NONE', #27603 ) ;
#72011=AXIS2_PLACEMENT_3D ( 'NONE', #90761, #121208, #34220 ) ;
#72048=EDGE_CURVE ( 'NONE', #123737, #30060, #35062, .T. ) ;
#72134=VERTEX_POINT ( 'NONE', #30483 ) ;
#72287=DIRECTION ( 'NONE',  ( -1.000000000000000000, 0.000000000000000000, 0.000000000000000000 ) ) ;
#72574=CARTESIAN_POINT ( 'NONE',  ( -1.055977286261792880, 0.8118917398807320440, 3.860134494607520672 ) ) ;
#73045=( NAMED_UNIT ( * ) SI_UNIT ( $, .STERADIAN. ) SOLID_ANGLE_UNIT ( ) );
#73250=CARTESIAN_POINT ( 'NONE',  ( -1.320800000000306618, -4.493284886149243553E-13, 3.775643966265820328 ) ) ;
#73412=CARTESIAN_POINT ( 'NONE',  ( 0.000000000000000000, -9.500000000000000000, 0.000000000000000000 ) ) ;
#73485=ADVANCED_FACE ( 'NONE', ( #3669 ), #23295, .F. ) ;
#74094=PRESENTATION_STYLE_ASSIGNMENT (( #128481 ) ) ;
#75891=CARTESIAN_POINT ( 'NONE',  ( 1.312016898163277157, 0.1750100709684468681, 3.778747987217102366 ) ) ;
#76296=ORIENTED_EDGE ( 'NONE', *, *, #54153, .F. ) ;
#76364=CARTESIAN_POINT ( 'NONE',  ( -0.1743029876375435661, -1.312104359949140431, 3.997104869979374531 ) ) ;
#77125=CARTESIAN_POINT ( 'NONE',  ( 0.000000000000000000, 0.000000000000000000, 0.000000000000000000 ) ) ;
#77250=STYLED_ITEM ( 'NONE', ( #46749 ), #81158 ) ;
#77354=( GEOMETRIC_REPRESENTATION_CONTEXT ( 3 ) GLOBAL_UNCERTAINTY_ASSIGNED_CONTEXT ( ( #25688 ) ) GLOBAL_UNIT_ASSIGNED_CONTEXT ( ( #69170, #91621, #23500 ) ) REPRESENTATION_CONTEXT ( 'NONE', 'WORKASPACE' ) );
#77355=CARTESIAN_POINT ( 'NONE',  ( 1.152381814940565130, 0.6684352261620748470, 3.831050770371648984 ) ) ;
#78372=CARTESIAN_POINT ( 'NONE',  ( 0.000000000000000000, -8.616843969807042924, 0.000000000000000000 ) ) ;
#78806=DIRECTION ( 'NONE',  ( -0.000000000000000000, 1.000000000000000000, -0.000000000000000000 ) ) ;
#78831=EDGE_CURVE ( 'NONE', #30060, #558, #125668, .T. ) ;
#79261=CARTESIAN_POINT ( 'NONE',  ( -0.4282563736389425890, -1.252432624735495326, 3.977822609706378909 ) ) ;
#79747=AXIS2_PLACEMENT_3D ( 'NONE', #15106, #37613, #47801 ) ;
#79820=ORIENTED_EDGE ( 'NONE', *, *, #3352, .T. ) ;
#79855=ORIENTED_EDGE ( 'NONE', *, *, #78831, .T. ) ;
#79937=ORIENTED_EDGE ( 'NONE', *, *, #109752, .F. ) ;
#80070=FACE_OUTER_BOUND ( 'NONE', #29774, .T. ) ;
#81158=ADVANCED_FACE ( 'NONE', ( #80070 ), #122088, .T. ) ;
#81314=AXIS2_PLACEMENT_3D ( 'NONE', #18870, #52905, #63134 ) ;
#81606=EDGE_CURVE ( 'NONE', #1799, #72134, #10235, .T. ) ;
#82346=EDGE_LOOP ( 'NONE', ( #143041, #36769, #84022, #62907, #104107, #56762, #96475, #19105, #105174 ) ) ;
#82466=EDGE_CURVE ( 'NONE', #48968, #58791, #83642, .T. ) ;
#83161=LINE ( 'NONE', #132417, #113812 ) ;
#83642=CIRCLE ( 'NONE', #95184, 4.000000000000000000 ) ;
#83751=SHAPE_DEFINITION_REPRESENTATION ( #65226, #118114 ) ;
#83861=DIRECTION ( 'NONE',  ( -0.000000000000000000, -0.000000000000000000, -1.000000000000000000 ) ) ;
#84022=ORIENTED_EDGE ( 'NONE', *, *, #1269, .F. ) ;
#84143=CARTESIAN_POINT ( 'NONE',  ( -1.277985381820198496, 0.3445797145511038106, 3.790392630796158624 ) ) ;
#84286=SURFACE_STYLE_FILL_AREA ( #63257 ) ;
#84290=DIRECTION ( 'NONE',  ( -0.000000000000000000, 1.000000000000000000, -0.000000000000000000 ) ) ;
#85766=CARTESIAN_POINT ( 'NONE',  ( 0.000000000000000000, 8.616843969807042924, 4.000000000000000000 ) ) ;
#86267=CARTESIAN_POINT ( 'NONE',  ( -0.5870628340341963458, 1.186303938595100860, 3.957500374151529332 ) ) ;
#88000=EDGE_CURVE ( 'NONE', #123737, #63821, #100565, .T. ) ;
#88344=AXIS2_PLACEMENT_3D ( 'NONE', #46617, #1584, #56041 ) ;
#88698=SURFACE_STYLE_USAGE ( .BOTH. , #32157 ) ;
#89656=COLOUR_RGB ( '', 0.66274510, 0.83137255, 0.94901961) ;
#90093=FILL_AREA_STYLE_COLOUR ( '', #140403 ) ;
#90761=CARTESIAN_POINT ( 'NONE',  ( 0.000000000000000000, -8.616843969807042924, 0.000000000000000000 ) ) ;
#91574=ORIENTED_EDGE ( 'NONE', *, *, #99598, .F. ) ;
#91621=( NAMED_UNIT ( * ) PLANE_ANGLE_UNIT ( ) SI_UNIT ( $, .RADIAN. ) );
#91932=MECHANICAL_DESIGN_GEOMETRIC_PRESENTATION_REPRESENTATION('',(#3930),#142954);
#92605=MANIFOLD_SOLID_BREP ( '#37 (0.104) Diameter Hole1', #46449 ) ;
#92729=ORIENTED_EDGE ( 'NONE', *, *, #43848, .T. ) ;
#92950=DIRECTION ( 'NONE',  ( -0.000000000000000000, -0.000000000000000000, -1.000000000000000000 ) ) ;
#93698=UNCERTAINTY_MEASURE_WITH_UNIT (LENGTH_MEASURE( 1.000000000000000082E-05 ), #43256, 'distance_accuracy_value', 'NONE');
#93819=CARTESIAN_POINT ( 'NONE',  ( 1.320799999999990870, 1.617513492313812843E-16, 0.000000000000000000 ) ) ;
#95184=AXIS2_PLACEMENT_3D ( 'NONE', #142305, #19778, #107506 ) ;
#95451=CARTESIAN_POINT ( 'NONE',  ( 0.1743335836340011991, -1.312101830529059265, 3.997104009112169010 ) ) ;
#95765=ORIENTED_EDGE ( 'NONE', *, *, #137581, .T. ) ;
#95849=ADVANCED_FACE ( 'NONE', ( #71535 ), #105550, .F. ) ;
#96160=( NAMED_UNIT ( * ) PLANE_ANGLE_UNIT ( ) SI_UNIT ( $, .RADIAN. ) );
#96475=ORIENTED_EDGE ( 'NONE', *, *, #13061, .T. ) ;
#96538=DIRECTION ( 'NONE',  ( 1.000000000000000000, 0.000000000000000000, 0.000000000000000000 ) ) ;
#97130=B_SPLINE_CURVE_WITH_KNOTS ( 'NONE', 3,
 ( #106538, #107959, #42052, #86267, #130487, #61668, #28315, #72574, #39926, #6490, #84143, #29016, #117416, #73250 ),
 .UNSPECIFIED., .F., .F.,
 ( 4, 2, 2, 2, 2, 2, 4 ),
 ( 0.004158817918585050455, 0.004678504169777139392, 0.004938347295373183427, 0.005198190420969228329, 0.005717876672161316398, 0.005977719797757361300, 0.006237562923353405335 ),
 .UNSPECIFIED. ) ;
#97225=( NAMED_UNIT ( * ) PLANE_ANGLE_UNIT ( ) SI_UNIT ( $, .RADIAN. ) );
#97738=CIRCLE ( 'NONE', #23754, 4.000000000000000000 ) ;
#98362=CARTESIAN_POINT ( 'NONE',  ( 1.055009550493547277, 0.8130331625670963458, 3.860388942535410539 ) ) ;
#99598=EDGE_CURVE ( 'NONE', #31655, #72010, #139433, .T. ) ;
#100565=CIRCLE ( 'NONE', #38071, 4.000000000000000000 ) ;
#100825=DIRECTION ( 'NONE',  ( 0.000000000000000000, 0.000000000000000000, 1.000000000000000000 ) ) ;
#100951=ORIENTED_EDGE ( 'NONE', *, *, #17009, .T. ) ;
#100976=STYLED_ITEM ( 'NONE', ( #132206 ), #121822 ) ;
#101120=ORIENTED_EDGE ( 'NONE', *, *, #7853, .T. ) ;
#101132=CIRCLE ( 'NONE', #103394, 4.000000000000000000 ) ;
#101774=SURFACE_STYLE_USAGE ( .BOTH. , #57591 ) ;
#102616=CIRCLE ( 'NONE', #118825, 9.500000000000000000 ) ;
#103394=AXIS2_PLACEMENT_3D ( 'NONE', #78372, #56662, #100825 ) ;
#103796=DIRECTION ( 'NONE',  ( 0.000000000000000000, 0.000000000000000000, 1.000000000000000000 ) ) ;
#104107=ORIENTED_EDGE ( 'NONE', *, *, #54153, .T. ) ;
#104330=EDGE_LOOP ( 'NONE', ( #133322, #129194 ) ) ;
#104973=APPLICATION_CONTEXT ( 'automotive_design' ) ;
#105174=ORIENTED_EDGE ( 'NONE', *, *, #66223, .F. ) ;
#105405=EDGE_LOOP ( 'NONE', ( #43306, #68062, #15865, #100951, #71566, #101120 ) ) ;
#105550=CYLINDRICAL_SURFACE ( 'NONE', #127047, 1.320799999999990870 ) ;
#105923=ORIENTED_EDGE ( 'NONE', *, *, #54166, .F. ) ;
#105992=CYLINDRICAL_SURFACE ( 'NONE', #43543, 4.000000000000000000 ) ;
#106293=CARTESIAN_POINT ( 'NONE',  ( 4.198949119135569656E-17, -1.320799999999990870, 4.000000000000000000 ) ) ;
#106538=CARTESIAN_POINT ( 'NONE',  ( -4.912274722134691121E-20, 1.320799999999990870, 4.000000000000000000 ) ) ;
#107041=CARTESIAN_POINT ( 'NONE',  ( 0.08796123503190976523, -1.320799999999990648, 4.000000000000000000 ) ) ;
#107506=DIRECTION ( 'NONE',  ( 0.000000000000000000, 0.000000000000000000, -1.000000000000000000 ) ) ;
#107757=PRESENTATION_STYLE_ASSIGNMENT (( #19344 ) ) ;
#107773=CARTESIAN_POINT ( 'NONE',  ( 1.320799999999990870, 1.617513596018363294E-16, 3.775643966265890494 ) ) ;
#107959=CARTESIAN_POINT ( 'NONE',  ( -0.1731940554707888380, 1.320799999999991092, 4.000000000000000000 ) ) ;
#108307=ORIENTED_EDGE ( 'NONE', *, *, #50976, .T. ) ;
#108770=DIRECTION ( 'NONE',  ( -0.000000000000000000, 1.000000000000000000, -0.000000000000000000 ) ) ;
#108953=CARTESIAN_POINT ( 'NONE',  ( -0.5879028318752435034, -1.185901033534117133, 3.957378740546157569 ) ) ;
#109223=CARTESIAN_POINT ( 'NONE',  ( 1.320799999999991092, 0.08682076437340231767, 3.775643966265890494 ) ) ;
#109752=EDGE_CURVE ( 'NONE', #23963, #42862, #62233, .T. ) ;
#110384=CARTESIAN_POINT ( 'NONE',  ( -1.285610022887904380, -0.3484131577337185037, 3.788408042242219054 ) ) ;
#110622=CARTESIAN_POINT ( 'NONE',  ( 0.1731953514540064132, 1.320799999999990648, 4.000000000000000000 ) ) ;
#110627=ORIENTED_EDGE ( 'NONE', *, *, #50976, .F. ) ;
#110728=ORIENTED_EDGE ( 'NONE', *, *, #71745, .T. ) ;
#111092=CARTESIAN_POINT ( 'NONE',  ( -0.8736642903051350384, -0.9942593280178064763, 3.903919091990571300 ) ) ;
#112000=MECHANICAL_DESIGN_GEOMETRIC_PRESENTATION_REPRESENTATION('',(#77250),#77354);
#113812=VECTOR ( 'NONE', #20740, 1000.000000000000000 ) ;
#113994=DIRECTION ( 'NONE',  ( -0.000000000000000000, 1.000000000000000000, -0.000000000000000000 ) ) ;
#114015=UNCERTAINTY_MEASURE_WITH_UNIT (LENGTH_MEASURE( 1.000000000000000082E-05 ), #4844, 'distance_accuracy_value', 'NONE');
#114417=CIRCLE ( 'NONE', #47421, 4.000000000000000000 ) ;
#115585=DIRECTION ( 'NONE',  ( 0.000000000000000000, -1.000000000000000000, 0.000000000000000000 ) ) ;
#116125=EDGE_LOOP ( 'NONE', ( #110627, #1358, #135427, #14969, #91574 ) ) ;
#117397=PRODUCT_DEFINITION ( 'UNKNOWN', '', #747, #140073 ) ;
#117416=CARTESIAN_POINT ( 'NONE',  ( -1.320800000000018404, 0.08703048564677724752, 3.775643966265881613 ) ) ;
#117576=DIRECTION ( 'NONE',  ( 0.000000000000000000, 0.000000000000000000, 1.000000000000000000 ) ) ;
#118114=SHAPE_REPRESENTATION ( '1.5 Handle Ball', ( #127880 ), #130349 ) ;
#118127=DIRECTION ( 'NONE',  ( -0.000000000000000000, -0.000000000000000000, -1.000000000000000000 ) ) ;
#118649=SURFACE_STYLE_FILL_AREA ( #44718 ) ;
#118825=AXIS2_PLACEMENT_3D ( 'NONE', #8109, #8793, #96538 ) ;
#120306=VECTOR ( 'NONE', #38731, 1000.000000000000000 ) ;
#120533=CARTESIAN_POINT ( 'NONE',  ( 4.198949119135569656E-17, -1.320799999999990870, 4.000000000000000000 ) ) ;
#120552=DIRECTION ( 'NONE',  ( 0.000000000000000000, 0.000000000000000000, -1.000000000000000000 ) ) ;
#120724=CARTESIAN_POINT ( 'NONE',  ( 1.320799999999990870, 1.617513596018363294E-16, 3.775643966265890494 ) ) ;
#120805=CARTESIAN_POINT ( 'NONE',  ( 0.5865329486478585430, 1.186553054598157964, 3.957575763987766670 ) ) ;
#121155=AXIS2_PLACEMENT_3D ( 'NONE', #59846, #115585, #27914 ) ;
#121208=DIRECTION ( 'NONE',  ( -0.000000000000000000, 1.000000000000000000, -0.000000000000000000 ) ) ;
#121822=ADVANCED_FACE ( 'NONE', ( #11079, #2347 ), #123485, .T. ) ;
#121978=CARTESIAN_POINT ( 'NONE',  ( -0.8062233626479216042, -1.049713688934361677, 3.918581274736450570 ) ) ;
#122088=SPHERICAL_SURFACE ( 'NONE', #811, 9.500000000000000000 ) ;
#122634=ORIENTED_EDGE ( 'NONE', *, *, #78831, .F. ) ;
#122705=CARTESIAN_POINT ( 'NONE',  ( -0.6634328256669722590, -1.145317346870745823, 3.945267063586698875 ) ) ;
#123485=SPHERICAL_SURFACE ( 'NONE', #33838, 9.500000000000000000 ) ;
#123737=VERTEX_POINT ( 'NONE', #17222 ) ;
#124202=ADVANCED_FACE ( 'NONE', ( #61832 ), #105992, .F. ) ;
#125668=CIRCLE ( 'NONE', #65571, 4.000000000000000000 ) ;
#125885=UNCERTAINTY_MEASURE_WITH_UNIT (LENGTH_MEASURE( 1.000000000000000082E-05 ), #196, 'distance_accuracy_value', 'NONE');
#126485=PRODUCT_CONTEXT ( 'NONE', #127200, 'mechanical' ) ;
#126640=CARTESIAN_POINT ( 'NONE',  ( 1.153529387357648650, -0.6659121308574033060, 3.830688525020676138 ) ) ;
#127047=AXIS2_PLACEMENT_3D ( 'NONE', #5521, #83861, #72287 ) ;
#127200=APPLICATION_CONTEXT ( 'automotive_design' ) ;
#127755=ORIENTED_EDGE ( 'NONE', *, *, #3268, .F. ) ;
#127880=AXIS2_PLACEMENT_3D ( 'NONE', #8925, #141658, #53195 ) ;
#128304=VECTOR ( 'NONE', #92950, 1000.000000000000000 ) ;
#128481=SURFACE_STYLE_USAGE ( .BOTH. , #129168 ) ;
#129168=SURFACE_SIDE_STYLE ('',( #84286 ) ) ;
#129194=ORIENTED_EDGE ( 'NONE', *, *, #81606, .T. ) ;
#129245=EDGE_CURVE ( 'NONE', #72134, #1799, #32775, .T. ) ;
#129496=CARTESIAN_POINT ( 'NONE',  ( 0.3440661715655736752, -1.278132184730745857, 3.986082177731342657 ) ) ;
#129565=ADVANCED_BREP_SHAPE_REPRESENTATION ( '', ( #92605, #127880 ), #130349 ) ;
#130349=( GEOMETRIC_REPRESENTATION_CONTEXT ( 3 ) GLOBAL_UNCERTAINTY_ASSIGNED_CONTEXT ( ( #114015 ) ) GLOBAL_UNIT_ASSIGNED_CONTEXT ( ( #4844, #96160, #73045 ) ) REPRESENTATION_CONTEXT ( 'NONE', 'WORKASPACE' ) );
#130487=CARTESIAN_POINT ( 'NONE',  ( -0.6643196045778319014, 1.144798890742325881, 3.945116340096009644 ) ) ;
#130639=( NAMED_UNIT ( * ) SI_UNIT ( $, .STERADIAN. ) SOLID_ANGLE_UNIT ( ) );
#131100=DIRECTION ( 'NONE',  ( 0.000000000000000000, 0.000000000000000000, -1.000000000000000000 ) ) ;
#131102=( GEOMETRIC_REPRESENTATION_CONTEXT ( 3 ) GLOBAL_UNCERTAINTY_ASSIGNED_CONTEXT ( ( #125885 ) ) GLOBAL_UNIT_ASSIGNED_CONTEXT ( ( #196, #54636, #33612 ) ) REPRESENTATION_CONTEXT ( 'NONE', 'WORKASPACE' ) );
#131899=VERTEX_POINT ( 'NONE', #4908 ) ;
#132206=PRESENTATION_STYLE_ASSIGNMENT (( #88698 ) ) ;
#132417=CARTESIAN_POINT ( 'NONE',  ( 0.000000000000000000, -9.500000000000000000, 4.000000000000000000 ) ) ;
#132913=CARTESIAN_POINT ( 'NONE',  ( -0.08791674731329272852, -1.320799999999990870, 4.000000000000001776 ) ) ;
#133322=ORIENTED_EDGE ( 'NONE', *, *, #129245, .T. ) ;
#135427=ORIENTED_EDGE ( 'NONE', *, *, #3268, .T. ) ;
#137581=EDGE_CURVE ( 'NONE', #4118, #558, #140084, .T. ) ;
#139433=B_SPLINE_CURVE_WITH_KNOTS ( 'NONE', 3,
 ( #107773, #109223, #75891, #9901, #52689, #77355, #98362, #43981, #33142, #8434, #120805, #22194, #110622, #55577 ),
 .UNSPECIFIED., .F., .F.,
 ( 4, 2, 2, 2, 2, 2, 4 ),
 ( 0.002080057358902690293, 0.002339902428862985096, 0.002599747498823280333, 0.003119437638743870374, 0.003379282708704165611, 0.003639127778664460414, 0.004158817918585050455 ),
 .UNSPECIFIED. ) ;
#139942=CYLINDRICAL_SURFACE ( 'NONE', #30957, 1.320799999999990870 ) ;
#140073=PRODUCT_DEFINITION_CONTEXT ( 'detailed design', #104973, 'design' ) ;
#140084=LINE ( 'NONE', #42199, #38890 ) ;
#140403=COLOUR_RGB ( '', 0.72549020, 0.75294118, 0.79215686) ;
#140613=FACE_OUTER_BOUND ( 'NONE', #15980, .T. ) ;
#141658=DIRECTION ( 'NONE',  ( 0.000000000000000000, 0.000000000000000000, 1.000000000000000000 ) ) ;
#142305=CARTESIAN_POINT ( 'NONE',  ( 0.000000000000000000, 8.616843969807042924, 0.000000000000000000 ) ) ;
#142564=SURFACE_SIDE_STYLE ('',( #118649 ) ) ;
#142795=CARTESIAN_POINT ( 'NONE',  ( 0.000000000000000000, -8.616843969807042924, 4.000000000000000000 ) ) ;
#142954=( GEOMETRIC_REPRESENTATION_CONTEXT ( 3 ) GLOBAL_UNCERTAINTY_ASSIGNED_CONTEXT ( ( #24273 ) ) GLOBAL_UNIT_ASSIGNED_CONTEXT ( ( #31307, #97225, #130639 ) ) REPRESENTATION_CONTEXT ( 'NONE', 'WORKASPACE' ) );
#143041=ORIENTED_EDGE ( 'NONE', *, *, #137581, .F. ) ;
ENDSEC;
END-ISO-10303-21;
